ISO-10303-21;
HEADER;
/* Generated by software containing ST-Developer
 * from STEP Tools, Inc. (www.steptools.com) 
 */

FILE_DESCRIPTION(
/* description */ ('Bin tilter linkage'),
/* implementation_level */ '2;1');

FILE_NAME(
/* name */ 'M4 short cap screw (11).step',
/* time_stamp */ '2026-10-28T03:26:24-07:00',
/* author */ (''),
/* organization */ (''),
/* preprocessor_version */ 'ST-DEVELOPER v20.2',
/* originating_system */ 'Autodesk Translation Framework v15.17.0.0',
/* authorisation */ '');

FILE_SCHEMA (('AUTOMOTIVE_DESIGN { 1 0 10303 214 3 1 1 }'));
ENDSEC;

DATA;
#10=MECHANICAL_DESIGN_GEOMETRIC_PRESENTATION_REPRESENTATION('',(#907),#23728);
#695=SHAPE_REPRESENTATION_RELATIONSHIP('SRR','None',#24160,#801);
#801=ADVANCED_BREP_SHAPE_REPRESENTATION('',(#1020),#23660);
#907=STYLED_ITEM('',(#24772),#1020);
#1020=MANIFOLD_SOLID_BREP('Body1',#12438);
#1295=FACE_BOUND('',#3220,.T.);
#1660=PLANE('',#14417);
#1661=PLANE('',#14422);
#1662=PLANE('',#14425);
#2234=FACE_OUTER_BOUND('',#3219,.T.);
#2235=FACE_OUTER_BOUND('',#3221,.T.);
#2236=FACE_OUTER_BOUND('',#3222,.T.);
#2237=FACE_OUTER_BOUND('',#3223,.T.);
#2238=FACE_OUTER_BOUND('',#3224,.T.);
#3219=EDGE_LOOP('',(#9697));
#3220=EDGE_LOOP('',(#9698));
#3221=EDGE_LOOP('',(#9699,#9700,#9701,#9702));
#3222=EDGE_LOOP('',(#9703));
#3223=EDGE_LOOP('',(#9704,#9705,#9706,#9707));
#3224=EDGE_LOOP('',(#9708));
#4163=LINE('',#21247,#4838);
#4164=LINE('',#21253,#4839);
#4838=VECTOR('',#17278,0.35);
#4839=VECTOR('',#17287,0.199999999999999);
#5547=CIRCLE('',#14418,0.35);
#5548=CIRCLE('',#14419,0.199999999999999);
#5549=CIRCLE('',#14421,0.35);
#5550=CIRCLE('',#14424,0.199999999999999);
#6397=VERTEX_POINT('',#21241);
#6398=VERTEX_POINT('',#21243);
#6399=VERTEX_POINT('',#21246);
#6400=VERTEX_POINT('',#21251);
#7588=EDGE_CURVE('',#6397,#6397,#5547,.T.);
#7589=EDGE_CURVE('',#6398,#6398,#5548,.T.);
#7590=EDGE_CURVE('',#6397,#6399,#4163,.T.);
#7591=EDGE_CURVE('',#6399,#6399,#5549,.T.);
#7592=EDGE_CURVE('',#6400,#6400,#5550,.T.);
#7593=EDGE_CURVE('',#6400,#6398,#4164,.T.);
#9697=ORIENTED_EDGE('',*,*,#7588,.T.);
#9698=ORIENTED_EDGE('',*,*,#7589,.F.);
#9699=ORIENTED_EDGE('',*,*,#7588,.F.);
#9700=ORIENTED_EDGE('',*,*,#7590,.T.);
#9701=ORIENTED_EDGE('',*,*,#7591,.T.);
#9702=ORIENTED_EDGE('',*,*,#7590,.F.);
#9703=ORIENTED_EDGE('',*,*,#7591,.F.);
#9704=ORIENTED_EDGE('',*,*,#7592,.F.);
#9705=ORIENTED_EDGE('',*,*,#7593,.T.);
#9706=ORIENTED_EDGE('',*,*,#7589,.T.);
#9707=ORIENTED_EDGE('',*,*,#7593,.F.);
#9708=ORIENTED_EDGE('',*,*,#7592,.T.);
#11439=CYLINDRICAL_SURFACE('',#14420,0.35);
#11440=CYLINDRICAL_SURFACE('',#14423,0.199999999999999);
#11959=ADVANCED_FACE('',(#2234,#1295),#1660,.T.);
#11960=ADVANCED_FACE('',(#2235),#11439,.T.);
#11961=ADVANCED_FACE('',(#2236),#1661,.F.);
#11962=ADVANCED_FACE('',(#2237),#11440,.T.);
#11963=ADVANCED_FACE('',(#2238),#1662,.T.);
#12438=CLOSED_SHELL('',(#11959,#11960,#11961,#11962,#11963));
#14416=AXIS2_PLACEMENT_3D('',#21239,#17268,#17269);
#14417=AXIS2_PLACEMENT_3D('',#21240,#17270,#17271);
#14418=AXIS2_PLACEMENT_3D('',#21242,#17272,#17273);
#14419=AXIS2_PLACEMENT_3D('',#21244,#17274,#17275);
#14420=AXIS2_PLACEMENT_3D('',#21245,#17276,#17277);
#14421=AXIS2_PLACEMENT_3D('',#21248,#17279,#17280);
#14422=AXIS2_PLACEMENT_3D('',#21249,#17281,#17282);
#14423=AXIS2_PLACEMENT_3D('',#21250,#17283,#17284);
#14424=AXIS2_PLACEMENT_3D('',#21252,#17285,#17286);
#14425=AXIS2_PLACEMENT_3D('',#21254,#17288,#17289);
#17268=DIRECTION('axis',(0.,0.,1.));
#17269=DIRECTION('refdir',(1.,0.,0.));
#17270=DIRECTION('center_axis',(0.,1.,0.));
#17271=DIRECTION('ref_axis',(1.,0.,0.));
#17272=DIRECTION('center_axis',(0.,1.,0.));
#17273=DIRECTION('ref_axis',(1.,0.,0.));
#17274=DIRECTION('center_axis',(0.,1.,0.));
#17275=DIRECTION('ref_axis',(1.,0.,0.));
#17276=DIRECTION('center_axis',(0.,1.,0.));
#17277=DIRECTION('ref_axis',(1.,0.,0.));
#17278=DIRECTION('',(0.,-1.,0.));
#17279=DIRECTION('center_axis',(0.,1.,0.));
#17280=DIRECTION('ref_axis',(1.,0.,0.));
#17281=DIRECTION('center_axis',(0.,1.,0.));
#17282=DIRECTION('ref_axis',(1.,0.,0.));
#17283=DIRECTION('center_axis',(0.,1.,0.));
#17284=DIRECTION('ref_axis',(1.,0.,0.));
#17285=DIRECTION('center_axis',(0.,1.,0.));
#17286=DIRECTION('ref_axis',(1.,0.,0.));
#17287=DIRECTION('',(0.,-1.,0.));
#17288=DIRECTION('center_axis',(0.,1.,0.));
#17289=DIRECTION('ref_axis',(1.,0.,0.));
#21239=CARTESIAN_POINT('',(0.,0.,0.));
#21240=CARTESIAN_POINT('Origin',(10.7050737530542,-0.8,17.1120538880616));
#21241=CARTESIAN_POINT('',(10.3550737530542,-0.8,17.1120538880616));
#21242=CARTESIAN_POINT('Origin',(10.7050737530542,-0.8,17.1120538880616));
#21243=CARTESIAN_POINT('',(10.5050737530542,-0.8,17.1120538880616));
#21244=CARTESIAN_POINT('Origin',(10.7050737530542,-0.8,17.1120538880616));
#21245=CARTESIAN_POINT('Origin',(10.7050737530542,-1.2,17.1120538880616));
#21246=CARTESIAN_POINT('',(10.3550737530542,-1.2,17.1120538880616));
#21247=CARTESIAN_POINT('',(10.3550737530542,-1.2,17.1120538880616));
#21248=CARTESIAN_POINT('Origin',(10.7050737530542,-1.2,17.1120538880616));
#21249=CARTESIAN_POINT('Origin',(10.7050737530542,-1.2,17.1120538880616));
#21250=CARTESIAN_POINT('Origin',(10.7050737530542,-0.8,17.1120538880616));
#21251=CARTESIAN_POINT('',(10.5050737530542,-0.1,17.1120538880616));
#21252=CARTESIAN_POINT('Origin',(10.7050737530542,-0.1,17.1120538880616));
#21253=CARTESIAN_POINT('',(10.5050737530542,-0.8,17.1120538880616));
#21254=CARTESIAN_POINT('Origin',(10.7050737530542,-0.1,17.1120538880616));
#23543=UNCERTAINTY_MEASURE_WITH_UNIT(LENGTH_MEASURE(0.001),#23729,
'DISTANCE_ACCURACY_VALUE',
'Maximum model space distance between geometric entities at asserted c
onnectivities');
#23611=UNCERTAINTY_MEASURE_WITH_UNIT(LENGTH_MEASURE(0.001),#23729,
'DISTANCE_ACCURACY_VALUE',
'Maximum model space distance between geometric entities at asserted c
onnectivities');
#23660=(
GEOMETRIC_REPRESENTATION_CONTEXT(3)
GLOBAL_UNCERTAINTY_ASSIGNED_CONTEXT((#23543))
GLOBAL_UNIT_ASSIGNED_CONTEXT((#23729,#23731,#23732))
REPRESENTATION_CONTEXT('','3D')
);
#23728=(
GEOMETRIC_REPRESENTATION_CONTEXT(3)
GLOBAL_UNCERTAINTY_ASSIGNED_CONTEXT((#23611))
GLOBAL_UNIT_ASSIGNED_CONTEXT((#23729,#23731,#23732))
REPRESENTATION_CONTEXT('','3D')
);
#23729=(
LENGTH_UNIT()
NAMED_UNIT(*)
SI_UNIT(.CENTI.,.METRE.)
);
#23731=(
NAMED_UNIT(*)
PLANE_ANGLE_UNIT()
SI_UNIT($,.RADIAN.)
);
#23732=(
NAMED_UNIT(*)
SI_UNIT($,.STERADIAN.)
SOLID_ANGLE_UNIT()
);
#23781=SHAPE_DEFINITION_REPRESENTATION(#23897,#24160);
#23897=PRODUCT_DEFINITION_SHAPE('',$,#24277);
#24160=SHAPE_REPRESENTATION('',(#14416),#23660);
#24228=PRODUCT_DEFINITION_CONTEXT('part definition',#24578,'design');
#24277=PRODUCT_DEFINITION('M4 short cap screw (11)',
'M4 short cap screw (11)',#24393,#24228);
#24393=PRODUCT_DEFINITION_FORMATION('',$,#24628);
#24578=APPLICATION_CONTEXT(
'Core Data for Automotive Mechanical Design Process');
#24579=PRODUCT_CONTEXT('part definition',#24578,'mechanical');
#24628=PRODUCT('M4 short cap screw (11)','M4 short cap screw (11)',
'M4 short cap screw (11)',(#24579));
#24766=COLOUR_RGB('Black',0.12,0.14,0.17);
#24767=FILL_AREA_STYLE_COLOUR('',#24766);
#24768=FILL_AREA_STYLE('',(#24767));
#24769=SURFACE_STYLE_FILL_AREA(#24768);
#24770=SURFACE_SIDE_STYLE('',(#24769));
#24771=SURFACE_STYLE_USAGE(.BOTH.,#24770);
#24772=PRESENTATION_STYLE_ASSIGNMENT((#24771));
ENDSEC;
END-ISO-10303-21;
